ISO-10303-21;
HEADER;
/* Generated by software containing ST-Developer
 * from STEP Tools, Inc. (www.steptools.com) 
 */

FILE_DESCRIPTION(
/* description */ (''),
/* implementation_level */ '2;1');

FILE_NAME(
/* name */ 'Blade_08.step',
/* time_stamp */ '2026-10-23T22:28:14+06:00',
/* author */ (''),
/* organization */ (''),
/* preprocessor_version */ 'ST-DEVELOPER v20.2',
/* originating_system */ 'Autodesk Translation Framework v15.15.0.0',
/* authorisation */ '');

FILE_SCHEMA (('AUTOMOTIVE_DESIGN { 1 0 10303 214 3 1 1 }'));
ENDSEC;

DATA;
#10=MECHANICAL_DESIGN_GEOMETRIC_PRESENTATION_REPRESENTATION('',(#114),#6753);
#88=SHAPE_REPRESENTATION_RELATIONSHIP('SRR','None',#6811,#101);
#101=ADVANCED_BREP_SHAPE_REPRESENTATION('',(#127),#6751);
#114=STYLED_ITEM('',(#6907),#127);
#127=MANIFOLD_SOLID_BREP('Blade_08',#3763);
#182=FACE_BOUND('',#795,.T.);
#183=FACE_BOUND('',#796,.T.);
#321=PLANE('',#4315);
#322=PLANE('',#4316);
#323=PLANE('',#4317);
#324=PLANE('',#4324);
#325=PLANE('',#4327);
#326=PLANE('',#4332);
#526=FACE_OUTER_BOUND('',#792,.T.);
#527=FACE_OUTER_BOUND('',#793,.T.);
#528=FACE_OUTER_BOUND('',#794,.T.);
#529=FACE_OUTER_BOUND('',#797,.T.);
#530=FACE_OUTER_BOUND('',#798,.T.);
#531=FACE_OUTER_BOUND('',#799,.T.);
#532=FACE_OUTER_BOUND('',#800,.T.);
#533=FACE_OUTER_BOUND('',#801,.T.);
#534=FACE_OUTER_BOUND('',#802,.T.);
#535=FACE_OUTER_BOUND('',#803,.T.);
#792=EDGE_LOOP('',(#3406,#3407,#3408,#3409));
#793=EDGE_LOOP('',(#3410,#3411,#3412,#3413));
#794=EDGE_LOOP('',(#3414,#3415,#3416,#3417));
#795=EDGE_LOOP('',(#3418));
#796=EDGE_LOOP('',(#3419));
#797=EDGE_LOOP('',(#3420,#3421,#3422,#3423));
#798=EDGE_LOOP('',(#3424));
#799=EDGE_LOOP('',(#3425,#3426,#3427,#3428));
#800=EDGE_LOOP('',(#3429));
#801=EDGE_LOOP('',(#3430,#3431,#3432,#3433));
#802=EDGE_LOOP('',(#3434,#3435,#3436,#3437));
#803=EDGE_LOOP('',(#3438,#3439,#3440,#3441));
#1016=CIRCLE('',#4318,33.8);
#1017=CIRCLE('',#4319,4.99999999999999);
#1018=CIRCLE('',#4320,1.1);
#1019=CIRCLE('',#4321,1.1);
#1020=CIRCLE('',#4323,1.1);
#1021=CIRCLE('',#4326,1.1);
#1022=CIRCLE('',#4329,4.99999999999999);
#1023=CIRCLE('',#4331,33.8);
#1298=LINE('',#6633,#1584);
#1299=LINE('',#6635,#1585);
#1300=LINE('',#6637,#1586);
#1301=LINE('',#6638,#1587);
#1302=LINE('',#6642,#1588);
#1303=LINE('',#6644,#1589);
#1304=LINE('',#6646,#1590);
#1305=LINE('',#6647,#1591);
#1306=LINE('',#6658,#1592);
#1307=LINE('',#6663,#1593);
#1584=VECTOR('',#5445,10.);
#1585=VECTOR('',#5446,10.);
#1586=VECTOR('',#5447,10.);
#1587=VECTOR('',#5448,10.);
#1588=VECTOR('',#5451,10.);
#1589=VECTOR('',#5452,10.);
#1590=VECTOR('',#5453,10.);
#1591=VECTOR('',#5454,10.);
#1592=VECTOR('',#5469,1.1);
#1593=VECTOR('',#5476,1.1);
#1921=VERTEX_POINT('',#6631);
#1922=VERTEX_POINT('',#6632);
#1923=VERTEX_POINT('',#6634);
#1924=VERTEX_POINT('',#6636);
#1925=VERTEX_POINT('',#6640);
#1926=VERTEX_POINT('',#6641);
#1927=VERTEX_POINT('',#6643);
#1928=VERTEX_POINT('',#6645);
#1929=VERTEX_POINT('',#6651);
#1930=VERTEX_POINT('',#6653);
#1931=VERTEX_POINT('',#6656);
#1932=VERTEX_POINT('',#6661);
#2420=EDGE_CURVE('',#1921,#1922,#1298,.T.);
#2421=EDGE_CURVE('',#1923,#1921,#1299,.T.);
#2422=EDGE_CURVE('',#1924,#1923,#1300,.T.);
#2423=EDGE_CURVE('',#1922,#1924,#1301,.T.);
#2424=EDGE_CURVE('',#1925,#1926,#1302,.T.);
#2425=EDGE_CURVE('',#1927,#1925,#1303,.T.);
#2426=EDGE_CURVE('',#1928,#1927,#1304,.T.);
#2427=EDGE_CURVE('',#1926,#1928,#1305,.T.);
#2428=EDGE_CURVE('',#1925,#1922,#1016,.T.);
#2429=EDGE_CURVE('',#1921,#1926,#1017,.T.);
#2430=EDGE_CURVE('',#1929,#1929,#1018,.T.);
#2431=EDGE_CURVE('',#1930,#1930,#1019,.T.);
#2432=EDGE_CURVE('',#1931,#1931,#1020,.T.);
#2433=EDGE_CURVE('',#1931,#1929,#1306,.T.);
#2434=EDGE_CURVE('',#1932,#1932,#1021,.T.);
#2435=EDGE_CURVE('',#1932,#1930,#1307,.T.);
#2436=EDGE_CURVE('',#1923,#1928,#1022,.T.);
#2437=EDGE_CURVE('',#1927,#1924,#1023,.T.);
#3406=ORIENTED_EDGE('',*,*,#2420,.F.);
#3407=ORIENTED_EDGE('',*,*,#2421,.F.);
#3408=ORIENTED_EDGE('',*,*,#2422,.F.);
#3409=ORIENTED_EDGE('',*,*,#2423,.F.);
#3410=ORIENTED_EDGE('',*,*,#2424,.F.);
#3411=ORIENTED_EDGE('',*,*,#2425,.F.);
#3412=ORIENTED_EDGE('',*,*,#2426,.F.);
#3413=ORIENTED_EDGE('',*,*,#2427,.F.);
#3414=ORIENTED_EDGE('',*,*,#2420,.T.);
#3415=ORIENTED_EDGE('',*,*,#2428,.F.);
#3416=ORIENTED_EDGE('',*,*,#2424,.T.);
#3417=ORIENTED_EDGE('',*,*,#2429,.F.);
#3418=ORIENTED_EDGE('',*,*,#2430,.T.);
#3419=ORIENTED_EDGE('',*,*,#2431,.T.);
#3420=ORIENTED_EDGE('',*,*,#2432,.F.);
#3421=ORIENTED_EDGE('',*,*,#2433,.T.);
#3422=ORIENTED_EDGE('',*,*,#2430,.F.);
#3423=ORIENTED_EDGE('',*,*,#2433,.F.);
#3424=ORIENTED_EDGE('',*,*,#2432,.T.);
#3425=ORIENTED_EDGE('',*,*,#2434,.F.);
#3426=ORIENTED_EDGE('',*,*,#2435,.T.);
#3427=ORIENTED_EDGE('',*,*,#2431,.F.);
#3428=ORIENTED_EDGE('',*,*,#2435,.F.);
#3429=ORIENTED_EDGE('',*,*,#2434,.T.);
#3430=ORIENTED_EDGE('',*,*,#2421,.T.);
#3431=ORIENTED_EDGE('',*,*,#2429,.T.);
#3432=ORIENTED_EDGE('',*,*,#2427,.T.);
#3433=ORIENTED_EDGE('',*,*,#2436,.F.);
#3434=ORIENTED_EDGE('',*,*,#2423,.T.);
#3435=ORIENTED_EDGE('',*,*,#2437,.F.);
#3436=ORIENTED_EDGE('',*,*,#2425,.T.);
#3437=ORIENTED_EDGE('',*,*,#2428,.T.);
#3438=ORIENTED_EDGE('',*,*,#2422,.T.);
#3439=ORIENTED_EDGE('',*,*,#2436,.T.);
#3440=ORIENTED_EDGE('',*,*,#2426,.T.);
#3441=ORIENTED_EDGE('',*,*,#2437,.T.);
#3531=CYLINDRICAL_SURFACE('',#4322,1.1);
#3532=CYLINDRICAL_SURFACE('',#4325,1.1);
#3533=CYLINDRICAL_SURFACE('',#4328,4.99999999999999);
#3534=CYLINDRICAL_SURFACE('',#4330,33.8);
#3732=ADVANCED_FACE('',(#526),#321,.F.);
#3733=ADVANCED_FACE('',(#527),#322,.F.);
#3734=ADVANCED_FACE('',(#528,#182,#183),#323,.F.);
#3735=ADVANCED_FACE('',(#529),#3531,.T.);
#3736=ADVANCED_FACE('',(#530),#324,.F.);
#3737=ADVANCED_FACE('',(#531),#3532,.T.);
#3738=ADVANCED_FACE('',(#532),#325,.F.);
#3739=ADVANCED_FACE('',(#533),#3533,.F.);
#3740=ADVANCED_FACE('',(#534),#3534,.T.);
#3741=ADVANCED_FACE('',(#535),#326,.T.);
#3763=CLOSED_SHELL('',(#3732,#3733,#3734,#3735,#3736,#3737,#3738,#3739,
#3740,#3741));
#4314=AXIS2_PLACEMENT_3D('',#6629,#5441,#5442);
#4315=AXIS2_PLACEMENT_3D('',#6630,#5443,#5444);
#4316=AXIS2_PLACEMENT_3D('',#6639,#5449,#5450);
#4317=AXIS2_PLACEMENT_3D('',#6648,#5455,#5456);
#4318=AXIS2_PLACEMENT_3D('',#6649,#5457,#5458);
#4319=AXIS2_PLACEMENT_3D('',#6650,#5459,#5460);
#4320=AXIS2_PLACEMENT_3D('',#6652,#5461,#5462);
#4321=AXIS2_PLACEMENT_3D('',#6654,#5463,#5464);
#4322=AXIS2_PLACEMENT_3D('',#6655,#5465,#5466);
#4323=AXIS2_PLACEMENT_3D('',#6657,#5467,#5468);
#4324=AXIS2_PLACEMENT_3D('',#6659,#5470,#5471);
#4325=AXIS2_PLACEMENT_3D('',#6660,#5472,#5473);
#4326=AXIS2_PLACEMENT_3D('',#6662,#5474,#5475);
#4327=AXIS2_PLACEMENT_3D('',#6664,#5477,#5478);
#4328=AXIS2_PLACEMENT_3D('',#6665,#5479,#5480);
#4329=AXIS2_PLACEMENT_3D('',#6666,#5481,#5482);
#4330=AXIS2_PLACEMENT_3D('',#6667,#5483,#5484);
#4331=AXIS2_PLACEMENT_3D('',#6668,#5485,#5486);
#4332=AXIS2_PLACEMENT_3D('',#6669,#5487,#5488);
#5441=DIRECTION('axis',(0.,0.,1.));
#5442=DIRECTION('refdir',(1.,0.,0.));
#5443=DIRECTION('center_axis',(3.88578058618805E-16,0.,1.));
#5444=DIRECTION('ref_axis',(1.,0.,-3.88578058618805E-16));
#5445=DIRECTION('',(1.,0.,-3.88578058618805E-16));
#5446=DIRECTION('',(0.,-1.,0.));
#5447=DIRECTION('',(-1.,0.,3.88578058618805E-16));
#5448=DIRECTION('',(0.,1.,0.));
#5449=DIRECTION('center_axis',(0.707106781186547,0.,-0.707106781186548));
#5450=DIRECTION('ref_axis',(-0.707106781186548,0.,-0.707106781186547));
#5451=DIRECTION('',(-0.707106781186548,0.,-0.707106781186547));
#5452=DIRECTION('',(0.,-1.,0.));
#5453=DIRECTION('',(0.707106781186548,0.,0.707106781186547));
#5454=DIRECTION('',(0.,1.,0.));
#5455=DIRECTION('center_axis',(0.,1.,0.));
#5456=DIRECTION('ref_axis',(0.707106781186547,0.,-0.707106781186548));
#5457=DIRECTION('center_axis',(0.,1.,0.));
#5458=DIRECTION('ref_axis',(0.707106781186547,0.,-0.707106781186548));
#5459=DIRECTION('center_axis',(0.,-1.,0.));
#5460=DIRECTION('ref_axis',(0.707106781186547,0.,-0.707106781186548));
#5461=DIRECTION('center_axis',(0.,1.,0.));
#5462=DIRECTION('ref_axis',(0.707106781186547,0.,-0.707106781186548));
#5463=DIRECTION('center_axis',(0.,1.,0.));
#5464=DIRECTION('ref_axis',(0.707106781186547,0.,-0.707106781186548));
#5465=DIRECTION('center_axis',(0.,-1.,0.));
#5466=DIRECTION('ref_axis',(0.707106781186547,0.,-0.707106781186548));
#5467=DIRECTION('center_axis',(0.,-1.,0.));
#5468=DIRECTION('ref_axis',(0.707106781186547,0.,-0.707106781186548));
#5469=DIRECTION('',(0.,1.,0.));
#5470=DIRECTION('center_axis',(0.,1.,0.));
#5471=DIRECTION('ref_axis',(0.707106781186547,0.,-0.707106781186548));
#5472=DIRECTION('center_axis',(0.,-1.,0.));
#5473=DIRECTION('ref_axis',(0.707106781186547,0.,-0.707106781186548));
#5474=DIRECTION('center_axis',(0.,-1.,0.));
#5475=DIRECTION('ref_axis',(0.707106781186547,0.,-0.707106781186548));
#5476=DIRECTION('',(0.,1.,0.));
#5477=DIRECTION('center_axis',(0.,1.,0.));
#5478=DIRECTION('ref_axis',(0.707106781186547,0.,-0.707106781186548));
#5479=DIRECTION('center_axis',(0.,1.,0.));
#5480=DIRECTION('ref_axis',(0.707106781186547,0.,-0.707106781186548));
#5481=DIRECTION('center_axis',(0.,-1.,0.));
#5482=DIRECTION('ref_axis',(0.707106781186547,0.,-0.707106781186548));
#5483=DIRECTION('center_axis',(0.,1.,0.));
#5484=DIRECTION('ref_axis',(0.707106781186547,0.,-0.707106781186548));
#5485=DIRECTION('center_axis',(0.,1.,0.));
#5486=DIRECTION('ref_axis',(0.707106781186547,0.,-0.707106781186548));
#5487=DIRECTION('center_axis',(0.,1.,0.));
#5488=DIRECTION('ref_axis',(0.707106781186547,0.,-0.707106781186548));
#6629=CARTESIAN_POINT('',(0.,0.,0.));
#6630=CARTESIAN_POINT('Origin',(4.99999999999998,-3.,114.33240815703));
#6631=CARTESIAN_POINT('',(4.99999999999998,-3.,114.33240815703));
#6632=CARTESIAN_POINT('',(33.8,-3.,114.33240815703));
#6633=CARTESIAN_POINT('',(2.5,-3.,114.33240815703));
#6634=CARTESIAN_POINT('',(4.99999999999998,-2.9,114.33240815703));
#6635=CARTESIAN_POINT('',(4.99999999999998,-3.,114.33240815703));
#6636=CARTESIAN_POINT('',(33.8,-2.9,114.33240815703));
#6637=CARTESIAN_POINT('',(2.5,-2.9,114.33240815703));
#6638=CARTESIAN_POINT('',(33.8,-3.,114.33240815703));
#6639=CARTESIAN_POINT('Origin',(23.9002092041053,-3.,138.232617361136));
#6640=CARTESIAN_POINT('',(23.9002092041053,-3.,138.232617361136));
#6641=CARTESIAN_POINT('',(3.53553390593273,-3.,117.867942062963));
#6642=CARTESIAN_POINT('',(11.9501046020526,-3.,126.282512759083));
#6643=CARTESIAN_POINT('',(23.9002092041053,-2.9,138.232617361136));
#6644=CARTESIAN_POINT('',(23.9002092041053,-3.,138.232617361136));
#6645=CARTESIAN_POINT('',(3.53553390593273,-2.9,117.867942062963));
#6646=CARTESIAN_POINT('',(11.9501046020526,-2.9,126.282512759083));
#6647=CARTESIAN_POINT('',(3.53553390593273,-3.,117.867942062963));
#6648=CARTESIAN_POINT('Origin',(0.,-3.,114.33240815703));
#6649=CARTESIAN_POINT('Origin',(0.,-3.,114.33240815703));
#6650=CARTESIAN_POINT('Origin',(0.,-3.,114.33240815703));
#6651=CARTESIAN_POINT('',(23.8644576694173,-3.,130.836708333491));
#6652=CARTESIAN_POINT('Origin',(24.6422751287225,-3.,130.058890874186));
#6653=CARTESIAN_POINT('',(28.0069405518647,-3.,120.209410689563));
#6654=CARTESIAN_POINT('Origin',(28.7847580111699,-3.,119.431593230258));
#6655=CARTESIAN_POINT('Origin',(24.6422751287225,-3.,130.058890874186));
#6656=CARTESIAN_POINT('',(23.8644576694173,-3.5,130.836708333491));
#6657=CARTESIAN_POINT('Origin',(24.6422751287225,-3.5,130.058890874186));
#6658=CARTESIAN_POINT('',(23.8644576694173,-3.,130.836708333491));
#6659=CARTESIAN_POINT('Origin',(24.6422751287225,-3.5,130.058890874186));
#6660=CARTESIAN_POINT('Origin',(28.7847580111699,-3.,119.431593230258));
#6661=CARTESIAN_POINT('',(28.0069405518647,-3.5,120.209410689563));
#6662=CARTESIAN_POINT('Origin',(28.7847580111699,-3.5,119.431593230258));
#6663=CARTESIAN_POINT('',(28.0069405518647,-3.,120.209410689563));
#6664=CARTESIAN_POINT('Origin',(28.7847580111699,-3.5,119.431593230258));
#6665=CARTESIAN_POINT('Origin',(0.,-3.,114.33240815703));
#6666=CARTESIAN_POINT('Origin',(0.,-2.9,114.33240815703));
#6667=CARTESIAN_POINT('Origin',(0.,-3.,114.33240815703));
#6668=CARTESIAN_POINT('Origin',(0.,-2.9,114.33240815703));
#6669=CARTESIAN_POINT('Origin',(0.,-2.9,114.33240815703));
#6736=UNCERTAINTY_MEASURE_WITH_UNIT(LENGTH_MEASURE(0.01),#6754,
'DISTANCE_ACCURACY_VALUE',
'Maximum model space distance between geometric entities at asserted c
onnectivities');
#6738=UNCERTAINTY_MEASURE_WITH_UNIT(LENGTH_MEASURE(0.01),#6754,
'DISTANCE_ACCURACY_VALUE',
'Maximum model space distance between geometric entities at asserted c
onnectivities');
#6751=(
GEOMETRIC_REPRESENTATION_CONTEXT(3)
GLOBAL_UNCERTAINTY_ASSIGNED_CONTEXT((#6736))
GLOBAL_UNIT_ASSIGNED_CONTEXT((#6754,#6756,#6757))
REPRESENTATION_CONTEXT('','3D')
);
#6753=(
GEOMETRIC_REPRESENTATION_CONTEXT(3)
GLOBAL_UNCERTAINTY_ASSIGNED_CONTEXT((#6738))
GLOBAL_UNIT_ASSIGNED_CONTEXT((#6754,#6756,#6757))
REPRESENTATION_CONTEXT('','3D')
);
#6754=(
LENGTH_UNIT()
NAMED_UNIT(*)
SI_UNIT(.MILLI.,.METRE.)
);
#6756=(
NAMED_UNIT(*)
PLANE_ANGLE_UNIT()
SI_UNIT($,.RADIAN.)
);
#6757=(
NAMED_UNIT(*)
SI_UNIT($,.STERADIAN.)
SOLID_ANGLE_UNIT()
);
#6770=SHAPE_DEFINITION_REPRESENTATION(#6784,#6811);
#6784=PRODUCT_DEFINITION_SHAPE('',$,#6826);
#6811=SHAPE_REPRESENTATION('',(#4314),#6751);
#6813=PRODUCT_DEFINITION_CONTEXT('part definition',#6857,'design');
#6826=PRODUCT_DEFINITION('Blade_08','Blade_08',#6840,#6813);
#6840=PRODUCT_DEFINITION_FORMATION('',$,#6871);
#6857=APPLICATION_CONTEXT(
'Core Data for Automotive Mechanical Design Process');
#6858=PRODUCT_CONTEXT('part definition',#6857,'mechanical');
#6871=PRODUCT('Blade_08','Blade_08',$,(#6858));
#6901=COLOUR_RGB('Light Blue',0.38,0.62,0.78);
#6902=FILL_AREA_STYLE_COLOUR('',#6901);
#6903=FILL_AREA_STYLE('',(#6902));
#6904=SURFACE_STYLE_FILL_AREA(#6903);
#6905=SURFACE_SIDE_STYLE('',(#6904));
#6906=SURFACE_STYLE_USAGE(.BOTH.,#6905);
#6907=PRESENTATION_STYLE_ASSIGNMENT((#6906));
ENDSEC;
END-ISO-10303-21;
